ISO-10303-21;
HEADER;
FILE_DESCRIPTION (('STEP AP214'),
    '1' );
FILE_NAME ('Stud.step',
    '2026-10-09T10:51:02',
    ( '' ),
    ( '' ),
    'SwSTEP 2.0',
    'SolidWorks 2026',
    '' );
FILE_SCHEMA (( 'AUTOMOTIVE_DESIGN' ));
ENDSEC;

DATA;
#60=SHAPE_REPRESENTATION_RELATIONSHIP ( 'NONE' , 'NONE' ,  #16508, #4953 ) ;
#88=DIRECTION ( 'NONE',  ( 0.000000000000000000, 1.000000000000000000, 0.000000000000000000 ) ) ;
#177=CARTESIAN_POINT ( 'NONE',  ( 79.99331838321626265, 102.0000000000000000, -1.033931352371318058 ) ) ;
#258=CARTESIAN_POINT ( 'NONE',  ( 79.99331838321626265, 54.99999999999999289, -1.033931352371318058 ) ) ;
#368=EDGE_CURVE ( 'NONE', #10057, #21384, #12802, .T. ) ;
#378=ADVANCED_FACE ( 'NONE', ( #6928 ), #5321, .T. ) ;
#394=DIRECTION ( 'NONE',  ( 0.000000000000000000, -0.000000000000000000, 1.000000000000000000 ) ) ;
#463=CARTESIAN_POINT ( 'NONE',  ( 79.99331838321626265, 100.9999999999999858, 4.966068647628683053 ) ) ;
#551=CARTESIAN_POINT ( 'NONE',  ( 79.99331838321626265, 100.9999999999999858, -1.033931352371318058 ) ) ;
#788=CIRCLE ( 'NONE', #20946, 4.999999999999994671 ) ;
#837=FACE_OUTER_BOUND ( 'NONE', #2752, .T. ) ;
#937=CARTESIAN_POINT ( 'NONE',  ( 79.99331838321626265, 102.0000000000000000, -1.033931352371318058 ) ) ;
#1191=AXIS2_PLACEMENT_3D ( 'NONE', #2311, #2185, #19538 ) ;
#1359=ADVANCED_FACE ( 'NONE', ( #837 ), #7833, .T. ) ;
#1395=DIRECTION ( 'NONE',  ( 1.000000000000000000, 0.000000000000000000, 0.000000000000000000 ) ) ;
#1619=CARTESIAN_POINT ( 'NONE',  ( 79.99331838321626265, 102.0000000000000000, -1.033931352371318058 ) ) ;
#1624=ADVANCED_FACE ( 'NONE', ( #12415 ), #9070, .T. ) ;
#1951=EDGE_LOOP ( 'NONE', ( #2676, #18595, #18575, #10980 ) ) ;
#1957=DIRECTION ( 'NONE',  ( 0.000000000000000000, 0.000000000000000000, -1.000000000000000000 ) ) ;
#1969=DIRECTION ( 'NONE',  ( -0.000000000000000000, -1.000000000000000000, -0.000000000000000000 ) ) ;
#2185=DIRECTION ( 'NONE',  ( -0.000000000000000000, -1.000000000000000000, -0.000000000000000000 ) ) ;
#2209=MANIFOLD_SOLID_BREP ( 'Stock-MAS-425-1', #9133 ) ;
#2273=CONICAL_SURFACE ( 'NONE', #20606, 4.999999999999997335, 0.7853981633974496113 ) ;
#2311=CARTESIAN_POINT ( 'NONE',  ( 79.99331838321626265, 54.99999999999999289, -1.033931352371318058 ) ) ;
#2475=ADVANCED_FACE ( 'NONE', ( #5384 ), #5281, .T. ) ;
#2489=DIRECTION ( 'NONE',  ( 0.000000000000000000, -0.000000000000000000, 1.000000000000000000 ) ) ;
#2676=ORIENTED_EDGE ( 'NONE', *, *, #20858, .F. ) ;
#2718=LINE ( 'NONE', #9477, #19906 ) ;
#2752=EDGE_LOOP ( 'NONE', ( #19574, #8834, #13343, #4593 ) ) ;
#2840=CARTESIAN_POINT ( 'NONE',  ( 79.99331838321626265, 102.0000000000000000, 4.966068647628683053 ) ) ;
#2885=DIRECTION ( 'NONE',  ( -0.000000000000000000, 1.000000000000000000, -0.000000000000000000 ) ) ;
#2947=( NAMED_UNIT ( * ) SI_UNIT ( $, .STERADIAN. ) SOLID_ANGLE_UNIT ( ) );
#3102=CARTESIAN_POINT ( 'NONE',  ( 0.000000000000000000, 0.000000000000000000, 0.000000000000000000 ) ) ;
#3113=DIRECTION ( 'NONE',  ( 0.000000000000000000, 0.000000000000000000, 1.000000000000000000 ) ) ;
#3150=CARTESIAN_POINT ( 'NONE',  ( 79.99331838321626265, 102.0000000000000000, -1.033931352371318058 ) ) ;
#3259=CARTESIAN_POINT ( 'NONE',  ( 79.99331838321626265, 55.99999999999999289, -7.033931352371318724 ) ) ;
#3293=CARTESIAN_POINT ( 'NONE',  ( 79.99331838321626265, 55.99999999999999289, 4.966068647628683053 ) ) ;
#3422=DIRECTION ( 'NONE',  ( 0.000000000000000000, 0.7071067811865456854, 0.7071067811865493491 ) ) ;
#3674=VECTOR ( 'NONE', #3422, 1000.000000000000000 ) ;
#3684=CARTESIAN_POINT ( 'NONE',  ( 79.99331838321626265, 102.0000000000000000, 3.966068647628679500 ) ) ;
#4361=DIRECTION ( 'NONE',  ( -0.000000000000000000, -1.000000000000000000, -0.000000000000000000 ) ) ;
#4467=ORIENTED_EDGE ( 'NONE', *, *, #19647, .F. ) ;
#4515=AXIS2_PLACEMENT_3D ( 'NONE', #3150, #12121, #8319 ) ;
#4593=ORIENTED_EDGE ( 'NONE', *, *, #14843, .T. ) ;
#4826=CONICAL_SURFACE ( 'NONE', #10363, 6.000000000000000888, 0.7853981633974509435 ) ;
#4852=ORIENTED_EDGE ( 'NONE', *, *, #22479, .T. ) ;
#4913=CARTESIAN_POINT ( 'NONE',  ( 79.99331838321626265, 55.99999999999999289, -1.033931352371318058 ) ) ;
#4953=ADVANCED_BREP_SHAPE_REPRESENTATION ( '', ( #2209, #6292 ), #6306 ) ;
#5157=VERTEX_POINT ( 'NONE', #11906 ) ;
#5281=CYLINDRICAL_SURFACE ( 'NONE', #20486, 6.000000000000000888 ) ;
#5306=VERTEX_POINT ( 'NONE', #3684 ) ;
#5313=UNCERTAINTY_MEASURE_WITH_UNIT (LENGTH_MEASURE( 1.000000000000000082E-05 ), #15714, 'distance_accuracy_value', 'NONE');
#5321=PLANE ( 'NONE',  #13171 ) ;
#5355=PRODUCT ( 'Stud', 'Stud', '', ( #15404 ) ) ;
#5384=FACE_OUTER_BOUND ( 'NONE', #10532, .T. ) ;
#5513=FACE_OUTER_BOUND ( 'NONE', #1951, .T. ) ;
#5521=DIRECTION ( 'NONE',  ( -0.000000000000000000, -1.000000000000000000, -0.000000000000000000 ) ) ;
#5534=EDGE_CURVE ( 'NONE', #5157, #21384, #16335, .T. ) ;
#5583=CIRCLE ( 'NONE', #19524, 6.000000000000000888 ) ;
#5611=CARTESIAN_POINT ( 'NONE',  ( 79.99331838321626265, 102.0000000000000000, -7.033931352371318724 ) ) ;
#5623=EDGE_CURVE ( 'NONE', #21384, #11064, #21341, .T. ) ;
#5737=CARTESIAN_POINT ( 'NONE',  ( 79.99331838321626265, 55.99999999999999289, -1.033931352371318058 ) ) ;
#5782=PRODUCT_DEFINITION ( 'UNKNOWN', '', #20169, #12262 ) ;
#6048=AXIS2_PLACEMENT_3D ( 'NONE', #13497, #11764, #20589 ) ;
#6077=ORIENTED_EDGE ( 'NONE', *, *, #7562, .T. ) ;
#6084=AXIS2_PLACEMENT_3D ( 'NONE', #15414, #12409, #10672 ) ;
#6147=ORIENTED_EDGE ( 'NONE', *, *, #19504, .T. ) ;
#6173=APPLICATION_CONTEXT ( 'automotive_design' ) ;
#6185=COLOUR_RGB ( '', 0.72549020, 0.75294118, 0.79215686) ;
#6228=VECTOR ( 'NONE', #11012, 1000.000000000000114 ) ;
#6292=AXIS2_PLACEMENT_3D ( 'NONE', #3102, #12069, #1395 ) ;
#6306=( GEOMETRIC_REPRESENTATION_CONTEXT ( 3 ) GLOBAL_UNCERTAINTY_ASSIGNED_CONTEXT ( ( #13220 ) ) GLOBAL_UNIT_ASSIGNED_CONTEXT ( ( #14442, #9114, #10518 ) ) REPRESENTATION_CONTEXT ( 'NONE', 'WORKASPACE' ) );
#6329=DIRECTION ( 'NONE',  ( 0.000000000000000000, 0.000000000000000000, -1.000000000000000000 ) ) ;
#6437=DIRECTION ( 'NONE',  ( -0.000000000000000000, 1.000000000000000000, -0.000000000000000000 ) ) ;
#6624=DIRECTION ( 'NONE',  ( -0.000000000000000000, -1.000000000000000000, -0.000000000000000000 ) ) ;
#6757=DIRECTION ( 'NONE',  ( 0.000000000000000000, 0.000000000000000000, 1.000000000000000000 ) ) ;
#6892=CARTESIAN_POINT ( 'NONE',  ( 79.99331838321626265, 102.0000000000000000, -1.033931352371318058 ) ) ;
#6928=FACE_OUTER_BOUND ( 'NONE', #10723, .T. ) ;
#6953=FILL_AREA_STYLE_COLOUR ( '', #6185 ) ;
#7171=DIRECTION ( 'NONE',  ( 0.000000000000000000, 1.000000000000000000, 0.000000000000000000 ) ) ;
#7258=ORIENTED_EDGE ( 'NONE', *, *, #9503, .T. ) ;
#7490=DIRECTION ( 'NONE',  ( 0.000000000000000000, 0.000000000000000000, -1.000000000000000000 ) ) ;
#7509=ADVANCED_FACE ( 'NONE', ( #5513 ), #4826, .T. ) ;
#7562=EDGE_CURVE ( 'NONE', #9818, #19234, #13318, .T. ) ;
#7626=ORIENTED_EDGE ( 'NONE', *, *, #5534, .F. ) ;
#7646=ORIENTED_EDGE ( 'NONE', *, *, #16709, .T. ) ;
#7771=CARTESIAN_POINT ( 'NONE',  ( 79.99331838321626265, 55.99999999999999289, 4.966068647628683053 ) ) ;
#7833=CYLINDRICAL_SURFACE ( 'NONE', #17545, 6.000000000000000888 ) ;
#8136=CIRCLE ( 'NONE', #12910, 6.000000000000000888 ) ;
#8318=DIRECTION ( 'NONE',  ( 0.000000000000000000, 0.000000000000000000, 1.000000000000000000 ) ) ;
#8319=DIRECTION ( 'NONE',  ( 0.000000000000000000, 0.000000000000000000, 1.000000000000000000 ) ) ;
#8430=LINE ( 'NONE', #3259, #10819 ) ;
#8488=EDGE_LOOP ( 'NONE', ( #20602, #6147, #18172, #7626 ) ) ;
#8792=PLANE ( 'NONE',  #20261 ) ;
#8834=ORIENTED_EDGE ( 'NONE', *, *, #368, .T. ) ;
#8956=ORIENTED_EDGE ( 'NONE', *, *, #12924, .T. ) ;
#9011=CONICAL_SURFACE ( 'NONE', #6084, 6.000000000000000888, 0.7853981633974509435 ) ;
#9070=CONICAL_SURFACE ( 'NONE', #13141, 4.999999999999997335, 0.7853981633974496113 ) ;
#9114=( NAMED_UNIT ( * ) PLANE_ANGLE_UNIT ( ) SI_UNIT ( $, .RADIAN. ) );
#9133=CLOSED_SHELL ( 'NONE', ( #1624, #10629, #2475, #1359, #378, #12287, #7509, #21761 ) ) ;
#9281=EDGE_CURVE ( 'NONE', #21384, #10057, #15100, .T. ) ;
#9320=DIRECTION ( 'NONE',  ( 0.000000000000000000, 0.000000000000000000, 1.000000000000000000 ) ) ;
#9465=ORIENTED_EDGE ( 'NONE', *, *, #19647, .T. ) ;
#9477=CARTESIAN_POINT ( 'NONE',  ( 79.99331838321626265, 102.0000000000000000, 3.966068647628679500 ) ) ;
#9496=STYLED_ITEM ( 'NONE', ( #12142 ), #2209 ) ;
#9503=EDGE_CURVE ( 'NONE', #5306, #5157, #18165, .T. ) ;
#9818=VERTEX_POINT ( 'NONE', #20100 ) ;
#9929=ORIENTED_EDGE ( 'NONE', *, *, #5623, .F. ) ;
#10057=VERTEX_POINT ( 'NONE', #463 ) ;
#10188=SURFACE_SIDE_STYLE ('',( #17316 ) ) ;
#10363=AXIS2_PLACEMENT_3D ( 'NONE', #5737, #17728, #21363 ) ;
#10472=DIRECTION ( 'NONE',  ( 0.000000000000000000, 0.000000000000000000, -1.000000000000000000 ) ) ;
#10518=( NAMED_UNIT ( * ) SI_UNIT ( $, .STERADIAN. ) SOLID_ANGLE_UNIT ( ) );
#10532=EDGE_LOOP ( 'NONE', ( #11008, #8956, #7646, #9929 ) ) ;
#10629=ADVANCED_FACE ( 'NONE', ( #19166 ), #9011, .T. ) ;
#10672=DIRECTION ( 'NONE',  ( 0.000000000000000000, 0.000000000000000000, 1.000000000000000000 ) ) ;
#10723=EDGE_LOOP ( 'NONE', ( #9465, #7258 ) ) ;
#10819=VECTOR ( 'NONE', #17086, 1000.000000000000000 ) ;
#10980=ORIENTED_EDGE ( 'NONE', *, *, #14843, .F. ) ;
#11008=ORIENTED_EDGE ( 'NONE', *, *, #9281, .T. ) ;
#11012=DIRECTION ( 'NONE',  ( 0.000000000000000000, -0.7071067811865465735, -0.7071067811865483499 ) ) ;
#11038=DIRECTION ( 'NONE',  ( 0.000000000000000000, -1.000000000000000000, 0.000000000000000000 ) ) ;
#11047=AXIS2_PLACEMENT_3D ( 'NONE', #551, #12392, #14232 ) ;
#11064=VERTEX_POINT ( 'NONE', #14660 ) ;
#11441=DIRECTION ( 'NONE',  ( 8.659560562354942719E-17, -0.7071067811865465735, 0.7071067811865483499 ) ) ;
#11583=LINE ( 'NONE', #2840, #14074 ) ;
#11667=DIRECTION ( 'NONE',  ( 0.000000000000000000, -1.000000000000000000, 0.000000000000000000 ) ) ;
#11764=DIRECTION ( 'NONE',  ( 0.000000000000000000, 1.000000000000000000, 0.000000000000000000 ) ) ;
#11838=SHAPE_DEFINITION_REPRESENTATION ( #15656, #16508 ) ;
#11902=CARTESIAN_POINT ( 'NONE',  ( 79.99331838321626265, 100.9999999999999858, -1.033931352371318058 ) ) ;
#11906=CARTESIAN_POINT ( 'NONE',  ( 79.99331838321626265, 102.0000000000000000, -6.033931352371315171 ) ) ;
#12041=LINE ( 'NONE', #3293, #3674 ) ;
#12069=DIRECTION ( 'NONE',  ( 0.000000000000000000, 0.000000000000000000, 1.000000000000000000 ) ) ;
#12121=DIRECTION ( 'NONE',  ( 0.000000000000000000, 1.000000000000000000, 0.000000000000000000 ) ) ;
#12142=PRESENTATION_STYLE_ASSIGNMENT (( #17436 ) ) ;
#12262=PRODUCT_DEFINITION_CONTEXT ( 'detailed design', #6173, 'design' ) ;
#12265=( NAMED_UNIT ( * ) PLANE_ANGLE_UNIT ( ) SI_UNIT ( $, .RADIAN. ) );
#12287=ADVANCED_FACE ( 'NONE', ( #19025 ), #8792, .F. ) ;
#12392=DIRECTION ( 'NONE',  ( 0.000000000000000000, -1.000000000000000000, 0.000000000000000000 ) ) ;
#12409=DIRECTION ( 'NONE',  ( -0.000000000000000000, 1.000000000000000000, -0.000000000000000000 ) ) ;
#12415=FACE_OUTER_BOUND ( 'NONE', #8488, .T. ) ;
#12802=CIRCLE ( 'NONE', #16842, 6.000000000000000888 ) ;
#12803=MECHANICAL_DESIGN_GEOMETRIC_PRESENTATION_REPRESENTATION('',(#9496),#22650);
#12910=AXIS2_PLACEMENT_3D ( 'NONE', #13578, #2885, #3113 ) ;
#12924=EDGE_CURVE ( 'NONE', #10057, #17159, #11583, .T. ) ;
#13029=CARTESIAN_POINT ( 'NONE',  ( 79.99331838321626265, 100.9999999999999858, -7.033931352371318724 ) ) ;
#13121=ORIENTED_EDGE ( 'NONE', *, *, #20858, .T. ) ;
#13141=AXIS2_PLACEMENT_3D ( 'NONE', #1619, #15877, #1957 ) ;
#13171=AXIS2_PLACEMENT_3D ( 'NONE', #177, #7171, #394 ) ;
#13220=UNCERTAINTY_MEASURE_WITH_UNIT (LENGTH_MEASURE( 1.000000000000000082E-05 ), #14442, 'distance_accuracy_value', 'NONE');
#13318=CIRCLE ( 'NONE', #1191, 4.999999999999994671 ) ;
#13343=ORIENTED_EDGE ( 'NONE', *, *, #5623, .T. ) ;
#13497=CARTESIAN_POINT ( 'NONE',  ( 79.99331838321626265, 102.0000000000000000, -1.033931352371318058 ) ) ;
#13578=CARTESIAN_POINT ( 'NONE',  ( 79.99331838321626265, 55.99999999999999289, -1.033931352371318058 ) ) ;
#14074=VECTOR ( 'NONE', #6624, 1000.000000000000000 ) ;
#14232=DIRECTION ( 'NONE',  ( 0.000000000000000000, 0.000000000000000000, 1.000000000000000000 ) ) ;
#14253=CARTESIAN_POINT ( 'NONE',  ( 79.99331838321626265, 102.0000000000000000, -6.033931352371315171 ) ) ;
#14442=( LENGTH_UNIT ( ) NAMED_UNIT ( * ) SI_UNIT ( .MILLI., .METRE. ) );
#14462=EDGE_LOOP ( 'NONE', ( #14626, #13121, #22506, #17935 ) ) ;
#14626=ORIENTED_EDGE ( 'NONE', *, *, #22479, .F. ) ;
#14660=CARTESIAN_POINT ( 'NONE',  ( 79.99331838321626265, 55.99999999999999289, -7.033931352371318724 ) ) ;
#14700=VECTOR ( 'NONE', #19719, 1000.000000000000000 ) ;
#14843=EDGE_CURVE ( 'NONE', #11064, #17159, #5583, .T. ) ;
#15002=ORIENTED_EDGE ( 'NONE', *, *, #368, .F. ) ;
#15100=CIRCLE ( 'NONE', #11047, 6.000000000000000888 ) ;
#15404=PRODUCT_CONTEXT ( 'NONE', #17182, 'mechanical' ) ;
#15414=CARTESIAN_POINT ( 'NONE',  ( 79.99331838321626265, 55.99999999999999289, -1.033931352371318058 ) ) ;
#15656=PRODUCT_DEFINITION_SHAPE ( 'NONE', 'NONE',  #5782 ) ;
#15714=( LENGTH_UNIT ( ) NAMED_UNIT ( * ) SI_UNIT ( .MILLI., .METRE. ) );
#15837=EDGE_CURVE ( 'NONE', #9818, #17159, #12041, .T. ) ;
#15845=CARTESIAN_POINT ( 'NONE',  ( 79.99331838321626265, 54.99999999999999289, -1.033931352371318058 ) ) ;
#15877=DIRECTION ( 'NONE',  ( 0.000000000000000000, -1.000000000000000000, 0.000000000000000000 ) ) ;
#16335=LINE ( 'NONE', #14253, #6228 ) ;
#16508=SHAPE_REPRESENTATION ( 'Stud', ( #6292 ), #6306 ) ;
#16540=CARTESIAN_POINT ( 'NONE',  ( 79.99331838321626265, 54.99999999999999289, -6.033931352371312506 ) ) ;
#16709=EDGE_CURVE ( 'NONE', #17159, #11064, #8136, .T. ) ;
#16842=AXIS2_PLACEMENT_3D ( 'NONE', #11902, #11667, #8318 ) ;
#17086=DIRECTION ( 'NONE',  ( 8.659560562354955045E-17, 0.7071067811865456854, -0.7071067811865493491 ) ) ;
#17159=VERTEX_POINT ( 'NONE', #7771 ) ;
#17182=APPLICATION_CONTEXT ( 'automotive_design' ) ;
#17316=SURFACE_STYLE_FILL_AREA ( #20967 ) ;
#17436=SURFACE_STYLE_USAGE ( .BOTH. , #10188 ) ;
#17545=AXIS2_PLACEMENT_3D ( 'NONE', #20096, #4361, #7490 ) ;
#17728=DIRECTION ( 'NONE',  ( -0.000000000000000000, 1.000000000000000000, -0.000000000000000000 ) ) ;
#17935=ORIENTED_EDGE ( 'NONE', *, *, #15837, .F. ) ;
#18089=EDGE_LOOP ( 'NONE', ( #6077, #4852 ) ) ;
#18165=CIRCLE ( 'NONE', #6048, 4.999999999999997335 ) ;
#18172=ORIENTED_EDGE ( 'NONE', *, *, #9281, .F. ) ;
#18277=FACE_OUTER_BOUND ( 'NONE', #21691, .T. ) ;
#18575=ORIENTED_EDGE ( 'NONE', *, *, #15837, .T. ) ;
#18595=ORIENTED_EDGE ( 'NONE', *, *, #7562, .F. ) ;
#19025=FACE_OUTER_BOUND ( 'NONE', #18089, .T. ) ;
#19166=FACE_OUTER_BOUND ( 'NONE', #14462, .T. ) ;
#19234=VERTEX_POINT ( 'NONE', #16540 ) ;
#19504=EDGE_CURVE ( 'NONE', #5306, #10057, #2718, .T. ) ;
#19524=AXIS2_PLACEMENT_3D ( 'NONE', #4913, #6437, #6757 ) ;
#19538=DIRECTION ( 'NONE',  ( 0.000000000000000000, 0.000000000000000000, 1.000000000000000000 ) ) ;
#19574=ORIENTED_EDGE ( 'NONE', *, *, #12924, .F. ) ;
#19647=EDGE_CURVE ( 'NONE', #5157, #5306, #22108, .T. ) ;
#19719=DIRECTION ( 'NONE',  ( -0.000000000000000000, -1.000000000000000000, -0.000000000000000000 ) ) ;
#19769=ORIENTED_EDGE ( 'NONE', *, *, #19504, .F. ) ;
#19819=ORIENTED_EDGE ( 'NONE', *, *, #5534, .T. ) ;
#19906=VECTOR ( 'NONE', #11441, 1000.000000000000114 ) ;
#20096=CARTESIAN_POINT ( 'NONE',  ( 79.99331838321626265, 102.0000000000000000, -1.033931352371318058 ) ) ;
#20100=CARTESIAN_POINT ( 'NONE',  ( 79.99331838321626265, 54.99999999999999289, 3.966068647628676835 ) ) ;
#20169=PRODUCT_DEFINITION_FORMATION_WITH_SPECIFIED_SOURCE ( 'ANY', '', #5355, .NOT_KNOWN. ) ;
#20261=AXIS2_PLACEMENT_3D ( 'NONE', #15845, #88, #2489 ) ;
#20486=AXIS2_PLACEMENT_3D ( 'NONE', #6892, #1969, #10472 ) ;
#20589=DIRECTION ( 'NONE',  ( 0.000000000000000000, 0.000000000000000000, 1.000000000000000000 ) ) ;
#20602=ORIENTED_EDGE ( 'NONE', *, *, #9503, .F. ) ;
#20606=AXIS2_PLACEMENT_3D ( 'NONE', #937, #11038, #6329 ) ;
#20858=EDGE_CURVE ( 'NONE', #19234, #11064, #8430, .T. ) ;
#20946=AXIS2_PLACEMENT_3D ( 'NONE', #258, #5521, #9320 ) ;
#20967=FILL_AREA_STYLE ('',( #6953 ) ) ;
#21341=LINE ( 'NONE', #5611, #14700 ) ;
#21363=DIRECTION ( 'NONE',  ( 0.000000000000000000, 0.000000000000000000, 1.000000000000000000 ) ) ;
#21384=VERTEX_POINT ( 'NONE', #13029 ) ;
#21691=EDGE_LOOP ( 'NONE', ( #19769, #4467, #19819, #15002 ) ) ;
#21761=ADVANCED_FACE ( 'NONE', ( #18277 ), #2273, .T. ) ;
#22108=CIRCLE ( 'NONE', #4515, 4.999999999999997335 ) ;
#22479=EDGE_CURVE ( 'NONE', #19234, #9818, #788, .T. ) ;
#22506=ORIENTED_EDGE ( 'NONE', *, *, #16709, .F. ) ;
#22650=( GEOMETRIC_REPRESENTATION_CONTEXT ( 3 ) GLOBAL_UNCERTAINTY_ASSIGNED_CONTEXT ( ( #5313 ) ) GLOBAL_UNIT_ASSIGNED_CONTEXT ( ( #15714, #12265, #2947 ) ) REPRESENTATION_CONTEXT ( 'NONE', 'WORKASPACE' ) );
ENDSEC;
END-ISO-10303-21;
